ISO-10303-21;
HEADER;
FILE_DESCRIPTION (('STEP AP214'),
    '1' );
FILE_NAME ('socket head cap screw_iso_ISO 4762 M5 x 20 - 20N.step',
    '2026-09-30T16:28:02',
    ( '' ),
    ( '' ),
    'SwSTEP 2.0',
    'SolidWorks 2026',
    '' );
FILE_SCHEMA (( 'AUTOMOTIVE_DESIGN' ));
ENDSEC;

DATA;
#17=AXIS2_PLACEMENT_3D ( 'NONE', #6944, #25711, #22673 ) ;
#103=EDGE_CURVE ( 'NONE', #184, #26603, #5846, .T. ) ;
#106=EDGE_CURVE ( 'NONE', #19956, #14105, #21866, .T. ) ;
#137=ORIENTED_EDGE ( 'NONE', *, *, #26787, .F. ) ;
#174=ORIENTED_EDGE ( 'NONE', *, *, #103, .T. ) ;
#184=VERTEX_POINT ( 'NONE', #293 ) ;
#293=CARTESIAN_POINT ( 'NONE',  ( 5.000000000000004441, 0.000000000000000000, 4.250000000000000000 ) ) ;
#302=ADVANCED_FACE ( 'NONE', ( #28256 ), #7306, .T. ) ;
#648=ADVANCED_FACE ( 'NONE', ( #29106 ), #6773, .F. ) ;
#700=CARTESIAN_POINT ( 'NONE',  ( 0.000000000000000000, 2.357898499370430834, -3.469446951953614189E-15 ) ) ;
#709=PLANE ( 'NONE',  #9392 ) ;
#720=CARTESIAN_POINT ( 'NONE',  ( 0.2500000000000002220, 5.204748896376250699E-16, -4.250000000000000000 ) ) ;
#789=CARTESIAN_POINT ( 'NONE',  ( 2.500000000000000444, -1.178949249685215417, 2.042000000000002036 ) ) ;
#871=CYLINDRICAL_SURFACE ( 'NONE', #19866, 2.500000000000000888 ) ;
#885=CIRCLE ( 'NONE', #17917, 4.250000000000000000 ) ;
#976=( NAMED_UNIT ( * ) SI_UNIT ( $, .STERADIAN. ) SOLID_ANGLE_UNIT ( ) );
#1004=EDGE_CURVE ( 'NONE', #7228, #23153, #12618, .T. ) ;
#1046=AXIS2_PLACEMENT_3D ( 'NONE', #21210, #26849, #5919 ) ;
#1053=VERTEX_POINT ( 'NONE', #14614 ) ;
#1080=EDGE_CURVE ( 'NONE', #23153, #15583, #23963, .T. ) ;
#1100=AXIS2_PLACEMENT_3D ( 'NONE', #1586, #6152, #22173 ) ;
#1119=DIRECTION ( 'NONE',  ( 0.000000000000000000, 0.000000000000000000, 1.000000000000000000 ) ) ;
#1121=CARTESIAN_POINT ( 'NONE',  ( 2.500000000000000444, 2.357898499370430834, -3.469446951953614189E-15 ) ) ;
#1133=ORIENTED_EDGE ( 'NONE', *, *, #2497, .F. ) ;
#1140=DIRECTION ( 'NONE',  ( 0.000000000000000000, 0.000000000000000000, 1.000000000000000000 ) ) ;
#1227=ORIENTED_EDGE ( 'NONE', *, *, #6644, .T. ) ;
#1292=ORIENTED_EDGE ( 'NONE', *, *, #6329, .F. ) ;
#1298=SURFACE_STYLE_USAGE ( .BOTH. , #24196 ) ;
#1398=VECTOR ( 'NONE', #14979, 1000.000000000000000 ) ;
#1445=CLOSED_SHELL ( 'NONE', ( #15132, #20882, #7737, #23190, #12590, #9060, #28804, #19502, #3783, #27996, #7327, #29752, #648, #8113, #11444, #4693, #302, #29167, #4024, #17444, #21025, #26089, #10107, #19688, #21517, #24283, #29171 ) ) ;
#1447=DIRECTION ( 'NONE',  ( 0.000000000000000000, 0.000000000000000000, 1.000000000000000000 ) ) ;
#1541=ORIENTED_EDGE ( 'NONE', *, *, #9804, .T. ) ;
#1586=CARTESIAN_POINT ( 'NONE',  ( 0.2500000000000002220, 0.000000000000000000, 0.000000000000000000 ) ) ;
#1603=VERTEX_POINT ( 'NONE', #18722 ) ;
#1610=ORIENTED_EDGE ( 'NONE', *, *, #14201, .F. ) ;
#1614=FACE_BOUND ( 'NONE', #16406, .T. ) ;
#1772=AXIS2_PLACEMENT_3D ( 'NONE', #8490, #29625, #19942 ) ;
#1846=ORIENTED_EDGE ( 'NONE', *, *, #20071, .F. ) ;
#1894=CYLINDRICAL_SURFACE ( 'NONE', #2902, 2.500000000000000888 ) ;
#1941=FACE_OUTER_BOUND ( 'NONE', #14215, .T. ) ;
#1943=CARTESIAN_POINT ( 'NONE',  ( 5.200000000000002842, 0.000000000000000000, -2.700000000000001066 ) ) ;
#1951=CONICAL_SURFACE ( 'NONE', #13612, 2.041999999999999815, 1.047197551196591858 ) ;
#1985=DIRECTION ( 'NONE',  ( 0.000000000000000000, -1.000000000000000000, 0.000000000000000000 ) ) ;
#2055=CARTESIAN_POINT ( 'NONE',  ( 2.500000000000000444, 2.357898499370430834, -3.469446951953614189E-15 ) ) ;
#2156=DIRECTION ( 'NONE',  ( -1.000000000000000000, 0.000000000000000000, 0.000000000000000000 ) ) ;
#2196=CARTESIAN_POINT ( 'NONE',  ( 2.500000000000000444, 2.357898499370430834, -3.469446951953614189E-15 ) ) ;
#2214=CIRCLE ( 'NONE', #10944, 4.000000000000000000 ) ;
#2448=AXIS2_PLACEMENT_3D ( 'NONE', #4691, #5148, #23620 ) ;
#2497=EDGE_CURVE ( 'NONE', #22465, #11088, #25074, .T. ) ;
#2509=ORIENTED_EDGE ( 'NONE', *, *, #10773, .F. ) ;
#2645=EDGE_CURVE ( 'NONE', #28670, #1603, #12057, .T. ) ;
#2682=VECTOR ( 'NONE', #25076, 1000.000000000000000 ) ;
#2708=DIRECTION ( 'NONE',  ( 0.000000000000000000, 1.000000000000000000, -1.471414886128461471E-15 ) ) ;
#2714=FACE_OUTER_BOUND ( 'NONE', #8518, .T. ) ;
#2729=CARTESIAN_POINT ( 'NONE',  ( 2.500000000000000444, -1.178949249685215417, 2.042000000000002036 ) ) ;
#2760=PLANE ( 'NONE',  #21921 ) ;
#2819=DIRECTION ( 'NONE',  ( 0.000000000000000000, 0.000000000000000000, 1.000000000000000000 ) ) ;
#2872=PLANE ( 'NONE',  #20969 ) ;
#2902=AXIS2_PLACEMENT_3D ( 'NONE', #11022, #11461, #9017 ) ;
#3012=AXIS2_PLACEMENT_3D ( 'NONE', #1943, #6054, #11227 ) ;
#3014=AXIS2_PLACEMENT_3D ( 'NONE', #15472, #3892, #22962 ) ;
#3052=DIRECTION ( 'NONE',  ( 0.000000000000000000, 0.000000000000000000, 1.000000000000000000 ) ) ;
#3078=ORIENTED_EDGE ( 'NONE', *, *, #28842, .F. ) ;
#3202=EDGE_CURVE ( 'NONE', #6766, #7950, #10617, .T. ) ;
#3298=PRESENTATION_STYLE_ASSIGNMENT (( #1298 ) ) ;
#3331=FACE_OUTER_BOUND ( 'NONE', #20608, .T. ) ;
#3388=FACE_OUTER_BOUND ( 'NONE', #18207, .T. ) ;
#3390=LINE ( 'NONE', #7954, #6688 ) ;
#3399=DIRECTION ( 'NONE',  ( 1.000000000000000000, 0.000000000000000000, 0.000000000000000000 ) ) ;
#3412=( LENGTH_UNIT ( ) NAMED_UNIT ( * ) SI_UNIT ( .MILLI., .METRE. ) );
#3455=STYLED_ITEM ( 'NONE', ( #3298 ), #11247 ) ;
#3458=DIRECTION ( 'NONE',  ( -1.000000000000000000, 0.000000000000000000, 0.000000000000000000 ) ) ;
#3470=ORIENTED_EDGE ( 'NONE', *, *, #5328, .T. ) ;
#3509=ORIENTED_EDGE ( 'NONE', *, *, #11404, .F. ) ;
#3585=( NAMED_UNIT ( * ) PLANE_ANGLE_UNIT ( ) SI_UNIT ( $, .RADIAN. ) );
#3634=DIRECTION ( 'NONE',  ( 0.000000000000000000, -0.4999999999999993894, 0.8660254037844389297 ) ) ;
#3682=ORIENTED_EDGE ( 'NONE', *, *, #1080, .F. ) ;
#3757=VERTEX_POINT ( 'NONE', #7996 ) ;
#3783=ADVANCED_FACE ( 'NONE', ( #17015 ), #22006, .T. ) ;
#3797=ORIENTED_EDGE ( 'NONE', *, *, #9804, .F. ) ;
#3844=ORIENTED_EDGE ( 'NONE', *, *, #1004, .T. ) ;
#3883=DIRECTION ( 'NONE',  ( 0.000000000000000000, 0.000000000000000000, 1.000000000000000000 ) ) ;
#3892=DIRECTION ( 'NONE',  ( 1.000000000000000000, 0.000000000000000000, 0.000000000000000000 ) ) ;
#3897=ORIENTED_EDGE ( 'NONE', *, *, #28842, .T. ) ;
#3903=VECTOR ( 'NONE', #6573, 1000.000000000000000 ) ;
#3907=ORIENTED_EDGE ( 'NONE', *, *, #25658, .T. ) ;
#3912=( GEOMETRIC_REPRESENTATION_CONTEXT ( 3 ) GLOBAL_UNCERTAINTY_ASSIGNED_CONTEXT ( ( #6760 ) ) GLOBAL_UNIT_ASSIGNED_CONTEXT ( ( #22024, #19422, #10411 ) ) REPRESENTATION_CONTEXT ( 'NONE', 'WORKASPACE' ) );
#3963=STYLED_ITEM ( 'NONE', ( #14685 ), #17465 ) ;
#3992=ORIENTED_EDGE ( 'NONE', *, *, #24358, .T. ) ;
#4024=ADVANCED_FACE ( 'NONE', ( #24878 ), #16148, .F. ) ;
#4074=DIRECTION ( 'NONE',  ( 0.000000000000000000, 0.000000000000000000, 1.000000000000000000 ) ) ;
#4152=DIRECTION ( 'NONE',  ( 0.000000000000000000, 0.000000000000000000, -1.000000000000000000 ) ) ;
#4312=DIRECTION ( 'NONE',  ( 0.000000000000000000, 0.000000000000000000, 1.000000000000000000 ) ) ;
#4313=FACE_OUTER_BOUND ( 'NONE', #20068, .T. ) ;
#4317=EDGE_CURVE ( 'NONE', #26921, #3757, #22235, .T. ) ;
#4387=ORIENTED_EDGE ( 'NONE', *, *, #9586, .F. ) ;
#4477=ORIENTED_EDGE ( 'NONE', *, *, #6194, .F. ) ;
#4556=CARTESIAN_POINT ( 'NONE',  ( 2.500000000000000444, 1.178949249685215417, -2.042000000000002036 ) ) ;
#4579=LINE ( 'NONE', #4720, #3903 ) ;
#4691=CARTESIAN_POINT ( 'NONE',  ( 2.500000000000000444, -2.357898499370430834, 3.469446951953614189E-15 ) ) ;
#4693=ADVANCED_FACE ( 'NONE', ( #2714 ), #2872, .F. ) ;
#4717=CARTESIAN_POINT ( 'NONE',  ( 2.500000000000000444, 0.000000000000000000, 0.000000000000000000 ) ) ;
#4720=CARTESIAN_POINT ( 'NONE',  ( 2.500000000000000444, 1.178949249685215417, -2.042000000000002036 ) ) ;
#4726=LINE ( 'NONE', #6430, #14374 ) ;
#4762=DIRECTION ( 'NONE',  ( 0.000000000000000000, 1.000000000000000000, -1.471414886128461471E-15 ) ) ;
#4935=CARTESIAN_POINT ( 'NONE',  ( 2.500000000000000444, 2.357898499370430834, -3.469446951953614189E-15 ) ) ;
#4947=VECTOR ( 'NONE', #27878, 999.9999999999998863 ) ;
#5014=DIRECTION ( 'NONE',  ( 0.000000000000000000, 0.5000000000000011102, 0.8660254037844380415 ) ) ;
#5067=ORIENTED_EDGE ( 'NONE', *, *, #24358, .F. ) ;
#5082=EDGE_CURVE ( 'NONE', #16768, #26056, #11726, .T. ) ;
#5096=DIRECTION ( 'NONE',  ( 0.000000000000000000, 0.000000000000000000, 1.000000000000000000 ) ) ;
#5148=DIRECTION ( 'NONE',  ( 0.000000000000000000, 0.8660254037844390407, 0.4999999999999993339 ) ) ;
#5172=DIRECTION ( 'NONE',  ( 0.000000000000000000, -0.5000000000000012212, -0.8660254037844380415 ) ) ;
#5181=DIRECTION ( 'NONE',  ( 0.000000000000000000, 0.000000000000000000, 1.000000000000000000 ) ) ;
#5187=DIRECTION ( 'NONE',  ( 0.000000000000000000, 0.000000000000000000, 1.000000000000000000 ) ) ;
#5202=ORIENTED_EDGE ( 'NONE', *, *, #6602, .T. ) ;
#5279=ORIENTED_EDGE ( 'NONE', *, *, #16236, .T. ) ;
#5284=ORIENTED_EDGE ( 'NONE', *, *, #14359, .F. ) ;
#5286=VECTOR ( 'NONE', #16455, 1000.000000000000000 ) ;
#5305=CARTESIAN_POINT ( 'NONE',  ( 5.200000000000002842, 0.000000000000000000, 2.500000000000000888 ) ) ;
#5311=EDGE_LOOP ( 'NONE', ( #6369, #9791, #18350 ) ) ;
#5328=EDGE_CURVE ( 'NONE', #26561, #10839, #11667, .T. ) ;
#5408=VECTOR ( 'NONE', #24087, 1000.000000000000000 ) ;
#5435=CARTESIAN_POINT ( 'NONE',  ( 0.000000000000000000, 0.000000000000000000, 0.000000000000000000 ) ) ;
#5514=EDGE_LOOP ( 'NONE', ( #3897, #25611, #20574, #6740 ) ) ;
#5522=CARTESIAN_POINT ( 'NONE',  ( 2.500000000000000444, 1.178949249685215417, -2.042000000000002036 ) ) ;
#5562=DIRECTION ( 'NONE',  ( 0.000000000000000000, 0.000000000000000000, 1.000000000000000000 ) ) ;
#5592=DIRECTION ( 'NONE',  ( 0.000000000000000000, 0.5000000000000012212, 0.8660254037844380415 ) ) ;
#5753=EDGE_CURVE ( 'NONE', #22950, #14986, #22937, .T. ) ;
#5764=CARTESIAN_POINT ( 'NONE',  ( 5.000000000000000888, 0.000000000000000000, 0.000000000000000000 ) ) ;
#5793=EDGE_LOOP ( 'NONE', ( #21940, #27566, #3078, #19528 ) ) ;
#5846=LINE ( 'NONE', #10714, #1398 ) ;
#5871=PLANE ( 'NONE',  #30094 ) ;
#5899=CIRCLE ( 'NONE', #15128, 2.041999999999999815 ) ;
#5900=CARTESIAN_POINT ( 'NONE',  ( 2.500000000000000444, -1.178949249685215417, 2.042000000000002036 ) ) ;
#5919=DIRECTION ( 'NONE',  ( 0.000000000000000000, -1.224646799147353454E-16, 1.000000000000000000 ) ) ;
#5940=ORIENTED_EDGE ( 'NONE', *, *, #16236, .F. ) ;
#5953=ORIENTED_EDGE ( 'NONE', *, *, #5328, .F. ) ;
#6046=DIRECTION ( 'NONE',  ( 0.000000000000000000, -0.4999999999999993894, 0.8660254037844389297 ) ) ;
#6054=DIRECTION ( 'NONE',  ( 0.000000000000000000, -1.000000000000000000, 0.000000000000000000 ) ) ;
#6152=DIRECTION ( 'NONE',  ( -1.000000000000000000, 0.000000000000000000, 0.000000000000000000 ) ) ;
#6194=EDGE_CURVE ( 'NONE', #16074, #7950, #22613, .T. ) ;
#6282=DIRECTION ( 'NONE',  ( -1.000000000000000000, 0.000000000000000000, 0.000000000000000000 ) ) ;
#6303=ORIENTED_EDGE ( 'NONE', *, *, #10903, .F. ) ;
#6308=DIRECTION ( 'NONE',  ( -0.5000000000000051070, 1.060575238724903217E-16, -0.8660254037844355990 ) ) ;
#6329=EDGE_CURVE ( 'NONE', #11088, #10839, #5899, .T. ) ;
#6369=ORIENTED_EDGE ( 'NONE', *, *, #1080, .T. ) ;
#6382=CARTESIAN_POINT ( 'NONE',  ( 0.000000000000000000, -1.178949249685215417, 2.042000000000002036 ) ) ;
#6408=DIRECTION ( 'NONE',  ( 0.000000000000000000, -1.287488025362403787E-15, -1.000000000000000000 ) ) ;
#6430=CARTESIAN_POINT ( 'NONE',  ( 2.500000000000000444, -1.178949249685215417, 2.042000000000002036 ) ) ;
#6491=VERTEX_POINT ( 'NONE', #19943 ) ;
#6573=DIRECTION ( 'NONE',  ( -1.000000000000000000, 0.000000000000000000, 0.000000000000000000 ) ) ;
#6602=EDGE_CURVE ( 'NONE', #14986, #26056, #21480, .T. ) ;
#6604=VECTOR ( 'NONE', #8778, 1000.000000000000000 ) ;
#6644=EDGE_CURVE ( 'NONE', #29341, #25494, #20021, .T. ) ;
#6688=VECTOR ( 'NONE', #14663, 1000.000000000000000 ) ;
#6740=ORIENTED_EDGE ( 'NONE', *, *, #25658, .F. ) ;
#6756=CARTESIAN_POINT ( 'NONE',  ( 2.500000000000000444, 0.000000000000000000, 0.000000000000000000 ) ) ;
#6758=CARTESIAN_POINT ( 'NONE',  ( -31.74999999999995737, 3.061616997868384127E-16, -2.500000000000000888 ) ) ;
#6760=UNCERTAINTY_MEASURE_WITH_UNIT (LENGTH_MEASURE( 1.000000000000000082E-05 ), #22024, 'distance_accuracy_value', 'NONE');
#6766=VERTEX_POINT ( 'NONE', #18406 ) ;
#6773=TOROIDAL_SURFACE ( 'NONE', #13099, 2.700000000000001066, 0.2000000000000000111 ) ;
#6784=CARTESIAN_POINT ( 'NONE',  ( -31.74999999999995737, 0.000000000000000000, 2.500000000000000888 ) ) ;
#6944=CARTESIAN_POINT ( 'NONE',  ( 5.200000000000002842, 0.000000000000000000, 0.000000000000000000 ) ) ;
#6945=VECTOR ( 'NONE', #15857, 1000.000000000000114 ) ;
#7188=DIRECTION ( 'NONE',  ( 0.000000000000000000, 0.000000000000000000, 1.000000000000000000 ) ) ;
#7198=EDGE_CURVE ( 'NONE', #6766, #22598, #12734, .T. ) ;
#7228=VERTEX_POINT ( 'NONE', #19454 ) ;
#7289=ORIENTED_EDGE ( 'NONE', *, *, #6644, .F. ) ;
#7306=PLANE ( 'NONE',  #27742 ) ;
#7311=ORIENTED_EDGE ( 'NONE', *, *, #10104, .F. ) ;
#7327=ADVANCED_FACE ( 'NONE', ( #1614, #11194 ), #13632, .T. ) ;
#7498=EDGE_CURVE ( 'NONE', #20489, #23153, #16227, .T. ) ;
#7575=TOROIDAL_SURFACE ( 'NONE', #15837, 4.000000000000000000, 0.2500000000000000000 ) ;
#7622=DIRECTION ( 'NONE',  ( -1.000000000000000000, 0.000000000000000000, 0.000000000000000000 ) ) ;
#7662=CARTESIAN_POINT ( 'NONE',  ( 3.678949249685231848, 0.000000000000000000, 0.000000000000000000 ) ) ;
#7663=EDGE_LOOP ( 'NONE', ( #9264, #4387, #21242, #26418, #3509, #10254 ) ) ;
#7737=ADVANCED_FACE ( 'NONE', ( #18533 ), #29300, .F. ) ;
#7759=VECTOR ( 'NONE', #14802, 1000.000000000000000 ) ;
#7803=CARTESIAN_POINT ( 'NONE',  ( 2.500000000000000444, 0.000000000000000000, 0.000000000000000000 ) ) ;
#7918=AXIS2_PLACEMENT_3D ( 'NONE', #16695, #16993, #13824 ) ;
#7933=CONICAL_SURFACE ( 'NONE', #13143, 2.055000000000000160, 0.7853981633974721488 ) ;
#7950=VERTEX_POINT ( 'NONE', #28346 ) ;
#7954=CARTESIAN_POINT ( 'NONE',  ( 0.000000000000000000, -2.357898499370430834, 3.469446951953614189E-15 ) ) ;
#7988=FACE_OUTER_BOUND ( 'NONE', #14792, .T. ) ;
#7996=CARTESIAN_POINT ( 'NONE',  ( 24.55500000000002103, 3.061616997868384620E-16, -2.500000000000001332 ) ) ;
#8023=AXIS2_PLACEMENT_3D ( 'NONE', #12116, #28950, #9672 ) ;
#8037=DIRECTION ( 'NONE',  ( -1.000000000000000000, -0.000000000000000000, -0.000000000000000000 ) ) ;
#8083=PRODUCT_CONTEXT ( 'NONE', #12991, 'mechanical' ) ;
#8113=ADVANCED_FACE ( 'NONE', ( #8130 ), #11779, .T. ) ;
#8130=FACE_OUTER_BOUND ( 'NONE', #24364, .T. ) ;
#8134=CARTESIAN_POINT ( 'NONE',  ( 2.500000000000000444, 0.000000000000000000, 2.041999999999999815 ) ) ;
#8212=ORIENTED_EDGE ( 'NONE', *, *, #2645, .T. ) ;
#8267=CARTESIAN_POINT ( 'NONE',  ( 5.000000000000002665, 0.000000000000000000, -2.700000000000001066 ) ) ;
#8299=( NAMED_UNIT ( * ) SI_UNIT ( $, .STERADIAN. ) SOLID_ANGLE_UNIT ( ) );
#8317=ORIENTED_EDGE ( 'NONE', *, *, #4317, .F. ) ;
#8434=CARTESIAN_POINT ( 'NONE',  ( 2.500000000000000444, 2.500728763858895382E-16, -2.041999999999999815 ) ) ;
#8459=EDGE_CURVE ( 'NONE', #10839, #28670, #21579, .T. ) ;
#8490=CARTESIAN_POINT ( 'NONE',  ( 5.000000000000004441, 0.000000000000000000, 0.000000000000000000 ) ) ;
#8518=EDGE_LOOP ( 'NONE', ( #10959, #4477, #137, #18115, #14886 ) ) ;
#8588=DIRECTION ( 'NONE',  ( 0.000000000000000000, 0.000000000000000000, -1.000000000000000000 ) ) ;
#8682=LINE ( 'NONE', #17989, #8689 ) ;
#8689=VECTOR ( 'NONE', #30113, 1000.000000000000000 ) ;
#8690=EDGE_CURVE ( 'NONE', #20489, #7228, #15711, .T. ) ;
#8705=CARTESIAN_POINT ( 'NONE',  ( 2.500000000000000444, 1.178949249685215417, 2.041999999999998483 ) ) ;
#8728=DIRECTION ( 'NONE',  ( 1.000000000000000000, -0.000000000000000000, -0.000000000000000000 ) ) ;
#8752=PRODUCT_DEFINITION_FORMATION_WITH_SPECIFIED_SOURCE ( 'ANY', '', #15688, .NOT_KNOWN. ) ;
#8778=DIRECTION ( 'NONE',  ( 0.000000000000000000, -1.000000000000000000, 1.287488025362403787E-15 ) ) ;
#8795=VECTOR ( 'NONE', #6282, 1000.000000000000000 ) ;
#8820=MECHANICAL_DESIGN_GEOMETRIC_PRESENTATION_REPRESENTATION('',(#3963),#3912);
#8823=DIRECTION ( 'NONE',  ( 0.000000000000000000, 1.000000000000000000, -1.287488025362403787E-15 ) ) ;
#8914=DIRECTION ( 'NONE',  ( 1.000000000000000000, 0.000000000000000000, 0.000000000000000000 ) ) ;
#9017=DIRECTION ( 'NONE',  ( 0.000000000000000000, 0.000000000000000000, 1.000000000000000000 ) ) ;
#9060=ADVANCED_FACE ( 'NONE', ( #29371 ), #7933, .T. ) ;
#9070=DIRECTION ( 'NONE',  ( 0.000000000000000000, 0.000000000000000000, -1.000000000000000000 ) ) ;
#9203=EDGE_CURVE ( 'NONE', #15583, #22598, #4579, .T. ) ;
#9225=AXIS2_PLACEMENT_3D ( 'NONE', #14627, #9445, #23975 ) ;
#9244=AXIS2_PLACEMENT_3D ( 'NONE', #21852, #17271, #1119 ) ;
#9257=FACE_OUTER_BOUND ( 'NONE', #25174, .T. ) ;
#9264=ORIENTED_EDGE ( 'NONE', *, *, #3202, .T. ) ;
#9392=AXIS2_PLACEMENT_3D ( 'NONE', #11988, #26059, #5592 ) ;
#9445=DIRECTION ( 'NONE',  ( -1.000000000000000000, 0.000000000000000000, 0.000000000000000000 ) ) ;
#9511=CIRCLE ( 'NONE', #26131, 0.2500000000000002220 ) ;
#9535=EDGE_LOOP ( 'NONE', ( #28748, #16427, #174, #20514 ) ) ;
#9562=FACE_OUTER_BOUND ( 'NONE', #19306, .T. ) ;
#9578=DIRECTION ( 'NONE',  ( -1.000000000000000000, 0.000000000000000000, 0.000000000000000000 ) ) ;
#9586=EDGE_CURVE ( 'NONE', #27772, #7950, #23613, .T. ) ;
#9666=ORIENTED_EDGE ( 'NONE', *, *, #26787, .T. ) ;
#9672=DIRECTION ( 'NONE',  ( 0.000000000000000000, 0.000000000000000000, -1.000000000000000000 ) ) ;
#9699=FACE_OUTER_BOUND ( 'NONE', #23943, .T. ) ;
#9723=ORIENTED_EDGE ( 'NONE', *, *, #28623, .T. ) ;
#9746=AXIS2_PLACEMENT_3D ( 'NONE', #30022, #23099, #11927 ) ;
#9791=ORIENTED_EDGE ( 'NONE', *, *, #10903, .T. ) ;
#9804=EDGE_CURVE ( 'NONE', #20489, #6766, #15904, .T. ) ;
#9812=ORIENTED_EDGE ( 'NONE', *, *, #18337, .T. ) ;
#9883=LINE ( 'NONE', #19195, #19140 ) ;
#10007=AXIS2_PLACEMENT_3D ( 'NONE', #16250, #29768, #9070 ) ;
#10049=FACE_OUTER_BOUND ( 'NONE', #21053, .T. ) ;
#10080=LINE ( 'NONE', #789, #14568 ) ;
#10084=DIRECTION ( 'NONE',  ( 0.000000000000000000, -0.5000000000000011102, -0.8660254037844379305 ) ) ;
#10104=EDGE_CURVE ( 'NONE', #28670, #26561, #19550, .T. ) ;
#10107=ADVANCED_FACE ( 'NONE', ( #3388 ), #24008, .F. ) ;
#10129=CARTESIAN_POINT ( 'NONE',  ( 5.200000000000002842, 0.000000000000000000, 0.000000000000000000 ) ) ;
#10246=LINE ( 'NONE', #19561, #16390 ) ;
#10254=ORIENTED_EDGE ( 'NONE', *, *, #7198, .F. ) ;
#10259=SHAPE_REPRESENTATION_RELATIONSHIP ( 'NONE' , 'NONE' ,  #11460, #17465 ) ;
#10360=CARTESIAN_POINT ( 'NONE',  ( 0.2500000000000002220, 0.000000000000000000, 0.000000000000000000 ) ) ;
#10411=( NAMED_UNIT ( * ) SI_UNIT ( $, .STERADIAN. ) SOLID_ANGLE_UNIT ( ) );
#10446=DIRECTION ( 'NONE',  ( 1.000000000000000000, 0.000000000000000000, 0.000000000000000000 ) ) ;
#10458=DIRECTION ( 'NONE',  ( 0.000000000000000000, 0.000000000000000000, 1.000000000000000000 ) ) ;
#10617=LINE ( 'NONE', #29291, #25299 ) ;
#10696=CARTESIAN_POINT ( 'NONE',  ( 2.500000000000000444, 2.357898499370430834, -3.469446951953614189E-15 ) ) ;
#10714=CARTESIAN_POINT ( 'NONE',  ( -31.74999999999995737, 0.000000000000000000, 4.250000000000000000 ) ) ;
#10731=CARTESIAN_POINT ( 'NONE',  ( 25.00000000000000000, 0.000000000000000000, 2.055000000000000160 ) ) ;
#10773=EDGE_CURVE ( 'NONE', #26056, #14986, #29060, .T. ) ;
#10803=VECTOR ( 'NONE', #11040, 1000.000000000000000 ) ;
#10839=VERTEX_POINT ( 'NONE', #25125 ) ;
#10903=EDGE_CURVE ( 'NONE', #15583, #11088, #15949, .T. ) ;
#10944=AXIS2_PLACEMENT_3D ( 'NONE', #12411, #14392, #5562 ) ;
#10959=ORIENTED_EDGE ( 'NONE', *, *, #9586, .T. ) ;
#11022=CARTESIAN_POINT ( 'NONE',  ( -31.74999999999995737, 0.000000000000000000, 0.000000000000000000 ) ) ;
#11040=DIRECTION ( 'NONE',  ( 0.000000000000000000, -1.000000000000000000, 1.287488025362403787E-15 ) ) ;
#11088=VERTEX_POINT ( 'NONE', #25728 ) ;
#11111=CIRCLE ( 'NONE', #16972, 2.500000000000000888 ) ;
#11194=FACE_OUTER_BOUND ( 'NONE', #15049, .T. ) ;
#11227=DIRECTION ( 'NONE',  ( 0.000000000000000000, 0.000000000000000000, -1.000000000000000000 ) ) ;
#11247=MANIFOLD_SOLID_BREP ( 'Hex', #1445 ) ;
#11335=DIRECTION ( 'NONE',  ( 0.000000000000000000, -0.8660254037844390407, -0.4999999999999994449 ) ) ;
#11404=EDGE_CURVE ( 'NONE', #22598, #28447, #23100, .T. ) ;
#11444=ADVANCED_FACE ( 'NONE', ( #25240 ), #18356, .T. ) ;
#11460=SHAPE_REPRESENTATION ( 'socket head cap screw_iso_ISO 4762 M5 x 20 - 20N', ( #13190 ), #21991 ) ;
#11461=DIRECTION ( 'NONE',  ( -1.000000000000000000, 0.000000000000000000, 0.000000000000000000 ) ) ;
#11515=DIRECTION ( 'NONE',  ( -1.000000000000000000, 0.000000000000000000, 0.000000000000000000 ) ) ;
#11520=DIRECTION ( 'NONE',  ( 0.000000000000000000, 0.000000000000000000, 1.000000000000000000 ) ) ;
#11588=ORIENTED_EDGE ( 'NONE', *, *, #10104, .T. ) ;
#11667=LINE ( 'NONE', #27902, #27405 ) ;
#11674=CARTESIAN_POINT ( 'NONE',  ( 0.000000000000000000, 0.000000000000000000, 0.000000000000000000 ) ) ;
#11726=CIRCLE ( 'NONE', #3012, 0.2000000000000000944 ) ;
#11779=TOROIDAL_SURFACE ( 'NONE', #1100, 4.000000000000000000, 0.2500000000000000000 ) ;
#11797=ORIENTED_EDGE ( 'NONE', *, *, #20705, .F. ) ;
#11809=CARTESIAN_POINT ( 'NONE',  ( 25.00000000000000000, 2.055000000000001492, 0.000000000000000000 ) ) ;
#11885=FACE_OUTER_BOUND ( 'NONE', #25961, .T. ) ;
#11927=DIRECTION ( 'NONE',  ( 0.000000000000000000, 1.224646799147353207E-16, 1.000000000000000000 ) ) ;
#11988=CARTESIAN_POINT ( 'NONE',  ( 2.500000000000000444, 2.357898499370430834, -3.469446951953614189E-15 ) ) ;
#12029=CARTESIAN_POINT ( 'NONE',  ( 2.500000000000000444, 2.357898499370430834, -3.469446951953614189E-15 ) ) ;
#12057=CIRCLE ( 'NONE', #27701, 2.041999999999999815 ) ;
#12084=ORIENTED_EDGE ( 'NONE', *, *, #13312, .F. ) ;
#12103=FACE_OUTER_BOUND ( 'NONE', #18746, .T. ) ;
#12116=CARTESIAN_POINT ( 'NONE',  ( 2.500000000000000444, 2.357898499370430834, -3.469446951953614189E-15 ) ) ;
#12174=CARTESIAN_POINT ( 'NONE',  ( 2.500000000000000444, -1.178949249685215417, -2.041999999999998483 ) ) ;
#12177=CARTESIAN_POINT ( 'NONE',  ( 25.00000000000000000, 0.000000000000000000, 0.000000000000000000 ) ) ;
#12192=CARTESIAN_POINT ( 'NONE',  ( 0.2500000000000002220, 0.000000000000000000, 0.000000000000000000 ) ) ;
#12294=ORIENTED_EDGE ( 'NONE', *, *, #27363, .F. ) ;
#12388=ORIENTED_EDGE ( 'NONE', *, *, #103, .F. ) ;
#12394=ORIENTED_EDGE ( 'NONE', *, *, #6602, .F. ) ;
#12398=DIRECTION ( 'NONE',  ( -1.000000000000000000, 0.000000000000000000, 0.000000000000000000 ) ) ;
#12411=CARTESIAN_POINT ( 'NONE',  ( 0.000000000000000000, 0.000000000000000000, 0.000000000000000000 ) ) ;
#12465=ORIENTED_EDGE ( 'NONE', *, *, #9203, .F. ) ;
#12590=ADVANCED_FACE ( 'NONE', ( #13053 ), #871, .T. ) ;
#12618=CIRCLE ( 'NONE', #19434, 2.041999999999999815 ) ;
#12681=DIRECTION ( 'NONE',  ( 0.000000000000000000, 0.000000000000000000, -1.000000000000000000 ) ) ;
#12734=LINE ( 'NONE', #700, #21500 ) ;
#12767=CARTESIAN_POINT ( 'NONE',  ( 24.55500000000002103, 0.000000000000000000, 2.500000000000001332 ) ) ;
#12858=EDGE_CURVE ( 'NONE', #16768, #22950, #11111, .T. ) ;
#12865=CARTESIAN_POINT ( 'NONE',  ( 0.2500000000000002220, 0.000000000000000000, 0.000000000000000000 ) ) ;
#12991=APPLICATION_CONTEXT ( 'automotive_design' ) ;
#13053=FACE_OUTER_BOUND ( 'NONE', #5514, .T. ) ;
#13099=AXIS2_PLACEMENT_3D ( 'NONE', #21739, #24337, #28959 ) ;
#13133=CIRCLE ( 'NONE', #9225, 2.500000000000001332 ) ;
#13143=AXIS2_PLACEMENT_3D ( 'NONE', #27373, #27220, #17698 ) ;
#13190=AXIS2_PLACEMENT_3D ( 'NONE', #5435, #19606, #10446 ) ;
#13216=DIRECTION ( 'NONE',  ( 1.000000000000000000, 0.000000000000000000, 0.000000000000000000 ) ) ;
#13312=EDGE_CURVE ( 'NONE', #26603, #29341, #885, .T. ) ;
#13338=LINE ( 'NONE', #6784, #23278 ) ;
#13374=VECTOR ( 'NONE', #10084, 1000.000000000000114 ) ;
#13390=APPLICATION_CONTEXT ( 'automotive_design' ) ;
#13467=ORIENTED_EDGE ( 'NONE', *, *, #20071, .T. ) ;
#13612=AXIS2_PLACEMENT_3D ( 'NONE', #14442, #21022, #23781 ) ;
#13632=PLANE ( 'NONE',  #3014 ) ;
#13636=DIRECTION ( 'NONE',  ( -1.000000000000000000, 0.000000000000000000, 0.000000000000000000 ) ) ;
#13666=CARTESIAN_POINT ( 'NONE',  ( 2.500000000000000444, 1.178949249685215417, -2.042000000000002036 ) ) ;
#13682=AXIS2_PLACEMENT_3D ( 'NONE', #5764, #8037, #14891 ) ;
#13749=PLANE ( 'NONE',  #27719 ) ;
#13824=DIRECTION ( 'NONE',  ( 0.000000000000000000, 0.000000000000000000, 1.000000000000000000 ) ) ;
#13988=ORIENTED_EDGE ( 'NONE', *, *, #18337, .F. ) ;
#14006=DIRECTION ( 'NONE',  ( -1.000000000000000000, 0.000000000000000000, 0.000000000000000000 ) ) ;
#14054=CARTESIAN_POINT ( 'NONE',  ( 5.000000000000004441, 0.000000000000000000, 0.000000000000000000 ) ) ;
#14070=VECTOR ( 'NONE', #5172, 999.9999999999998863 ) ;
#14105=VERTEX_POINT ( 'NONE', #12767 ) ;
#14145=MECHANICAL_DESIGN_GEOMETRIC_PRESENTATION_REPRESENTATION('',(#3455),#25382);
#14201=EDGE_CURVE ( 'NONE', #6491, #184, #20729, .T. ) ;
#14215=EDGE_LOOP ( 'NONE', ( #24994, #20536, #1292 ) ) ;
#14359=EDGE_CURVE ( 'NONE', #27706, #25494, #18827, .T. ) ;
#14374=VECTOR ( 'NONE', #27968, 1000.000000000000114 ) ;
#14392=DIRECTION ( 'NONE',  ( -1.000000000000000000, 0.000000000000000000, 0.000000000000000000 ) ) ;
#14426=EDGE_LOOP ( 'NONE', ( #24173, #28124, #21912 ) ) ;
#14442=CARTESIAN_POINT ( 'NONE',  ( 2.500000000000000444, 0.000000000000000000, 0.000000000000000000 ) ) ;
#14444=DIRECTION ( 'NONE',  ( 0.000000000000000000, 0.000000000000000000, -1.000000000000000000 ) ) ;
#14552=ORIENTED_EDGE ( 'NONE', *, *, #14359, .T. ) ;
#14568=VECTOR ( 'NONE', #4762, 1000.000000000000000 ) ;
#14584=CIRCLE ( 'NONE', #18014, 2.041999999999999815 ) ;
#14603=VECTOR ( 'NONE', #2708, 1000.000000000000000 ) ;
#14614=CARTESIAN_POINT ( 'NONE',  ( 0.000000000000000000, -2.357898499370430834, 3.469446951953614189E-15 ) ) ;
#14627=CARTESIAN_POINT ( 'NONE',  ( 24.55500000000002103, 0.000000000000000000, 0.000000000000000000 ) ) ;
#14663=DIRECTION ( 'NONE',  ( 0.000000000000000000, 0.4999999999999993339, -0.8660254037844390407 ) ) ;
#14672=ORIENTED_EDGE ( 'NONE', *, *, #5753, .F. ) ;
#14685=PRESENTATION_STYLE_ASSIGNMENT (( #26314 ) ) ;
#14763=VECTOR ( 'NONE', #24474, 1000.000000000000114 ) ;
#14792=EDGE_LOOP ( 'NONE', ( #9666, #19533, #28770 ) ) ;
#14802=DIRECTION ( 'NONE',  ( 0.000000000000000000, -1.000000000000000000, 1.287488025362403787E-15 ) ) ;
#14818=FACE_OUTER_BOUND ( 'NONE', #9535, .T. ) ;
#14841=CARTESIAN_POINT ( 'NONE',  ( 0.000000000000000000, 0.000000000000000000, 4.000000000000000000 ) ) ;
#14886=ORIENTED_EDGE ( 'NONE', *, *, #17750, .T. ) ;
#14891=DIRECTION ( 'NONE',  ( 0.000000000000000000, 0.000000000000000000, -1.000000000000000000 ) ) ;
#14930=AXIS2_PLACEMENT_3D ( 'NONE', #23876, #12398, #2819 ) ;
#14955=CARTESIAN_POINT ( 'NONE',  ( 2.500000000000000444, -1.178949249685215417, -2.041999999999998483 ) ) ;
#14979=DIRECTION ( 'NONE',  ( -1.000000000000000000, 0.000000000000000000, 0.000000000000000000 ) ) ;
#14986=VERTEX_POINT ( 'NONE', #23261 ) ;
#15008=( LENGTH_UNIT ( ) NAMED_UNIT ( * ) SI_UNIT ( .MILLI., .METRE. ) );
#15049=EDGE_LOOP ( 'NONE', ( #1846, #1610 ) ) ;
#15064=ORIENTED_EDGE ( 'NONE', *, *, #22835, .F. ) ;
#15093=EDGE_LOOP ( 'NONE', ( #5953, #7311, #20966 ) ) ;
#15103=COLOUR_RGB ( '', 0.40784314, 0.44705882, 0.49803922) ;
#15128=AXIS2_PLACEMENT_3D ( 'NONE', #25205, #18318, #7188 ) ;
#15132=ADVANCED_FACE ( 'NONE', ( #12103 ), #22267, .F. ) ;
#15134=DIRECTION ( 'NONE',  ( -0.7071067811865306973, 0.000000000000000000, 0.7071067811865643371 ) ) ;
#15345=EDGE_LOOP ( 'NONE', ( #8317, #5279, #26692, #20305 ) ) ;
#15472=CARTESIAN_POINT ( 'NONE',  ( 5.000000000000000888, 4.250000000000003553, 0.000000000000000000 ) ) ;
#15583=VERTEX_POINT ( 'NONE', #18031 ) ;
#15653=CARTESIAN_POINT ( 'NONE',  ( 2.500000000000000444, 2.357898499370430834, -3.469446951953614189E-15 ) ) ;
#15671=DIRECTION ( 'NONE',  ( 0.000000000000000000, -0.5000000000000011102, -0.8660254037844379305 ) ) ;
#15688=PRODUCT ( 'socket head cap screw_iso_ISO 4762 M5 x 20 - 20N', 'socket head cap screw_iso_ISO 4762 M5 x 20 - 20N', '', ( #8083 ) ) ;
#15711=LINE ( 'NONE', #25041, #6945 ) ;
#15738=CARTESIAN_POINT ( 'NONE',  ( 2.500000000000000444, 2.357898499370430834, -3.469446951953614189E-15 ) ) ;
#15760=DIRECTION ( 'NONE',  ( -1.000000000000000000, 0.000000000000000000, 0.000000000000000000 ) ) ;
#15819=AXIS2_PLACEMENT_3D ( 'NONE', #12865, #8728, #1140 ) ;
#15837=AXIS2_PLACEMENT_3D ( 'NONE', #12192, #23350, #5181 ) ;
#15857=DIRECTION ( 'NONE',  ( 0.000000000000000000, -0.4999999999999993894, 0.8660254037844389297 ) ) ;
#15900=LINE ( 'NONE', #6758, #2682 ) ;
#15904=LINE ( 'NONE', #2196, #17046 ) ;
#15917=EDGE_LOOP ( 'NONE', ( #14672, #28752, #19664, #12394 ) ) ;
#15936=VECTOR ( 'NONE', #6308, 1000.000000000000114 ) ;
#15949=LINE ( 'NONE', #13666, #6604 ) ;
#15953=CYLINDRICAL_SURFACE ( 'NONE', #19284, 4.250000000000000000 ) ;
#15995=ORIENTED_EDGE ( 'NONE', *, *, #22496, .F. ) ;
#16011=VECTOR ( 'NONE', #15671, 1000.000000000000114 ) ;
#16074=VERTEX_POINT ( 'NONE', #30114 ) ;
#16148=PLANE ( 'NONE',  #16647 ) ;
#16203=EDGE_LOOP ( 'NONE', ( #16287, #5940 ) ) ;
#16227=LINE ( 'NONE', #4935, #4947 ) ;
#16236=EDGE_CURVE ( 'NONE', #26921, #19956, #26942, .T. ) ;
#16250=CARTESIAN_POINT ( 'NONE',  ( 5.000000000000000888, 0.000000000000000000, 0.000000000000000000 ) ) ;
#16270=EDGE_CURVE ( 'NONE', #7228, #16074, #9883, .T. ) ;
#16281=DIRECTION ( 'NONE',  ( 0.000000000000000000, -1.000000000000000000, 1.471414886128461471E-15 ) ) ;
#16287=ORIENTED_EDGE ( 'NONE', *, *, #16736, .F. ) ;
#16302=DIRECTION ( 'NONE',  ( 0.000000000000000000, 0.000000000000000000, 1.000000000000000000 ) ) ;
#16390=VECTOR ( 'NONE', #29540, 1000.000000000000000 ) ;
#16406=EDGE_LOOP ( 'NONE', ( #20263, #5202 ) ) ;
#16427=ORIENTED_EDGE ( 'NONE', *, *, #14201, .T. ) ;
#16455=DIRECTION ( 'NONE',  ( -1.000000000000000000, 0.000000000000000000, 0.000000000000000000 ) ) ;
#16528=DIRECTION ( 'NONE',  ( 0.000000000000000000, 0.4999999999999993339, -0.8660254037844390407 ) ) ;
#16611=CARTESIAN_POINT ( 'NONE',  ( 2.500000000000000444, -1.178949249685215417, 2.042000000000002036 ) ) ;
#16647=AXIS2_PLACEMENT_3D ( 'NONE', #4556, #6408, #8823 ) ;
#16695=CARTESIAN_POINT ( 'NONE',  ( 2.500000000000000444, 0.000000000000000000, 0.000000000000000000 ) ) ;
#16728=EDGE_CURVE ( 'NONE', #1603, #7228, #22563, .T. ) ;
#16736=EDGE_CURVE ( 'NONE', #19956, #26921, #20592, .T. ) ;
#16763=CARTESIAN_POINT ( 'NONE',  ( 25.00000000000000000, 2.789133085058098087E-16, -2.055000000000000160 ) ) ;
#16768=VERTEX_POINT ( 'NONE', #24032 ) ;
#16815=ORIENTED_EDGE ( 'NONE', *, *, #3202, .F. ) ;
#16972=AXIS2_PLACEMENT_3D ( 'NONE', #20079, #8914, #18230 ) ;
#16978=DIRECTION ( 'NONE',  ( 0.000000000000000000, 0.000000000000000000, -1.000000000000000000 ) ) ;
#16988=SURFACE_SIDE_STYLE ('',( #26621 ) ) ;
#16993=DIRECTION ( 'NONE',  ( -1.000000000000000000, 0.000000000000000000, 0.000000000000000000 ) ) ;
#17015=FACE_OUTER_BOUND ( 'NONE', #15345, .T. ) ;
#17046=VECTOR ( 'NONE', #29566, 1000.000000000000000 ) ;
#17113=LINE ( 'NONE', #5522, #7759 ) ;
#17145=CARTESIAN_POINT ( 'NONE',  ( 25.00000000000000000, 0.000000000000000000, 0.000000000000000000 ) ) ;
#17251=SHAPE_DEFINITION_REPRESENTATION ( #19567, #11460 ) ;
#17271=DIRECTION ( 'NONE',  ( -1.000000000000000000, 0.000000000000000000, 0.000000000000000000 ) ) ;
#17286=FILL_AREA_STYLE ('',( #19573 ) ) ;
#17381=ORIENTED_EDGE ( 'NONE', *, *, #20705, .T. ) ;
#17444=ADVANCED_FACE ( 'NONE', ( #9699 ), #709, .F. ) ;
#17465=ADVANCED_BREP_SHAPE_REPRESENTATION ( '', ( #11247, #13190 ), #21991 ) ;
#17467=ORIENTED_EDGE ( 'NONE', *, *, #2497, .T. ) ;
#17606=SURFACE_STYLE_FILL_AREA ( #26646 ) ;
#17698=DIRECTION ( 'NONE',  ( 0.000000000000000000, 0.000000000000000000, 1.000000000000000000 ) ) ;
#17700=CARTESIAN_POINT ( 'NONE',  ( 0.000000000000000000, -1.178949249685215417, -2.041999999999998483 ) ) ;
#17750=EDGE_CURVE ( 'NONE', #25132, #27772, #24818, .T. ) ;
#17838=AXIS2_PLACEMENT_3D ( 'NONE', #1121, #3399, #16978 ) ;
#17904=CARTESIAN_POINT ( 'NONE',  ( 0.000000000000000000, 5.051668046482832750E-16, -4.000000000000000000 ) ) ;
#17917=AXIS2_PLACEMENT_3D ( 'NONE', #10360, #26263, #5187 ) ;
#17950=LINE ( 'NONE', #6382, #16011 ) ;
#17989=CARTESIAN_POINT ( 'NONE',  ( 2.500000000000000444, -1.178949249685215417, 2.042000000000002036 ) ) ;
#18014=AXIS2_PLACEMENT_3D ( 'NONE', #29840, #2156, #23057 ) ;
#18031=CARTESIAN_POINT ( 'NONE',  ( 2.500000000000000444, 1.178949249685215417, -2.042000000000002036 ) ) ;
#18115=ORIENTED_EDGE ( 'NONE', *, *, #28303, .F. ) ;
#18207=EDGE_LOOP ( 'NONE', ( #11797, #21108, #18892 ) ) ;
#18219=ORIENTED_EDGE ( 'NONE', *, *, #20034, .T. ) ;
#18230=DIRECTION ( 'NONE',  ( 0.000000000000000000, 0.000000000000000000, -1.000000000000000000 ) ) ;
#18318=DIRECTION ( 'NONE',  ( -1.000000000000000000, 0.000000000000000000, 0.000000000000000000 ) ) ;
#18337=EDGE_CURVE ( 'NONE', #22465, #1603, #29095, .T. ) ;
#18350=ORIENTED_EDGE ( 'NONE', *, *, #28623, .F. ) ;
#18356=PLANE ( 'NONE',  #27866 ) ;
#18404=ORIENTED_EDGE ( 'NONE', *, *, #24043, .T. ) ;
#18406=CARTESIAN_POINT ( 'NONE',  ( 0.000000000000000000, 2.357898499370430834, -3.469446951953614189E-15 ) ) ;
#18457=AXIS2_PLACEMENT_3D ( 'NONE', #19589, #28958, #1447 ) ;
#18533=FACE_OUTER_BOUND ( 'NONE', #28421, .T. ) ;
#18714=EDGE_LOOP ( 'NONE', ( #27782, #20321, #20288, #6303, #21972 ) ) ;
#18722=CARTESIAN_POINT ( 'NONE',  ( 2.500000000000000444, 0.000000000000000000, 2.042000000000002036 ) ) ;
#18746=EDGE_LOOP ( 'NONE', ( #13988, #17467, #20214, #26715, #8212 ) ) ;
#18827=CIRCLE ( 'NONE', #26139, 4.000000000000000000 ) ;
#18879=DIRECTION ( 'NONE',  ( 0.000000000000000000, 1.471414886128461471E-15, 1.000000000000000000 ) ) ;
#18892=ORIENTED_EDGE ( 'NONE', *, *, #2645, .F. ) ;
#19046=ORIENTED_EDGE ( 'NONE', *, *, #6194, .T. ) ;
#19050=LINE ( 'NONE', #12174, #5286 ) ;
#19086=AXIS2_PLACEMENT_3D ( 'NONE', #26338, #15760, #3883 ) ;
#19129=DIRECTION ( 'NONE',  ( -1.000000000000000000, 0.000000000000000000, 0.000000000000000000 ) ) ;
#19140=VECTOR ( 'NONE', #3634, 1000.000000000000114 ) ;
#19195=CARTESIAN_POINT ( 'NONE',  ( 2.500000000000000444, 2.357898499370430834, -3.469446951953614189E-15 ) ) ;
#19212=DIRECTION ( 'NONE',  ( 0.000000000000000000, 0.000000000000000000, 1.000000000000000000 ) ) ;
#19277=ORIENTED_EDGE ( 'NONE', *, *, #20034, .F. ) ;
#19284=AXIS2_PLACEMENT_3D ( 'NONE', #25130, #11515, #4074 ) ;
#19306=EDGE_LOOP ( 'NONE', ( #15995, #5067, #3470, #18404, #25307 ) ) ;
#19335=ORIENTED_EDGE ( 'NONE', *, *, #5753, .T. ) ;
#19389=DIRECTION ( 'NONE',  ( -1.000000000000000000, 0.000000000000000000, 0.000000000000000000 ) ) ;
#19422=( NAMED_UNIT ( * ) PLANE_ANGLE_UNIT ( ) SI_UNIT ( $, .RADIAN. ) );
#19434=AXIS2_PLACEMENT_3D ( 'NONE', #4717, #14006, #3052 ) ;
#19441=DIRECTION ( 'NONE',  ( 1.000000000000000000, 0.000000000000000000, 0.000000000000000000 ) ) ;
#19454=CARTESIAN_POINT ( 'NONE',  ( 2.500000000000000444, 1.768423874527823347, 1.020999999999997687 ) ) ;
#19502=ADVANCED_FACE ( 'NONE', ( #23121 ), #25416, .T. ) ;
#19528=ORIENTED_EDGE ( 'NONE', *, *, #106, .F. ) ;
#19533=ORIENTED_EDGE ( 'NONE', *, *, #16270, .F. ) ;
#19550=LINE ( 'NONE', #24293, #13374 ) ;
#19561=CARTESIAN_POINT ( 'NONE',  ( 2.500000000000000444, -2.357898499370430834, 3.469446951953614189E-15 ) ) ;
#19567=PRODUCT_DEFINITION_SHAPE ( 'NONE', 'NONE',  #27455 ) ;
#19573=FILL_AREA_STYLE_COLOUR ( '', #22960 ) ;
#19589=CARTESIAN_POINT ( 'NONE',  ( 24.55500000000002103, 0.000000000000000000, 0.000000000000000000 ) ) ;
#19606=DIRECTION ( 'NONE',  ( 0.000000000000000000, 0.000000000000000000, 1.000000000000000000 ) ) ;
#19664=ORIENTED_EDGE ( 'NONE', *, *, #5082, .T. ) ;
#19688=ADVANCED_FACE ( 'NONE', ( #7988 ), #21433, .F. ) ;
#19735=DIRECTION ( 'NONE',  ( 1.000000000000000000, 0.000000000000000000, 0.000000000000000000 ) ) ;
#19821=EDGE_CURVE ( 'NONE', #25494, #27706, #2214, .T. ) ;
#19866=AXIS2_PLACEMENT_3D ( 'NONE', #26516, #22376, #10458 ) ;
#19889=FACE_OUTER_BOUND ( 'NONE', #14426, .T. ) ;
#19942=DIRECTION ( 'NONE',  ( 0.000000000000000000, 0.000000000000000000, 1.000000000000000000 ) ) ;
#19943=CARTESIAN_POINT ( 'NONE',  ( 5.000000000000004441, 5.204748896376250699E-16, -4.250000000000000000 ) ) ;
#19956=VERTEX_POINT ( 'NONE', #10731 ) ;
#20021=CIRCLE ( 'NONE', #1046, 0.2500000000000002220 ) ;
#20025=CARTESIAN_POINT ( 'NONE',  ( 25.00000000000000000, 0.000000000000000000, 2.055000000000000160 ) ) ;
#20034=EDGE_CURVE ( 'NONE', #29341, #26603, #26564, .T. ) ;
#20068=EDGE_LOOP ( 'NONE', ( #22816, #26730, #3907, #21307 ) ) ;
#20071=EDGE_CURVE ( 'NONE', #184, #6491, #28551, .T. ) ;
#20076=EDGE_CURVE ( 'NONE', #3757, #16768, #15900, .T. ) ;
#20079=CARTESIAN_POINT ( 'NONE',  ( 5.200000000000002842, 0.000000000000000000, 0.000000000000000000 ) ) ;
#20092=CARTESIAN_POINT ( 'NONE',  ( 2.500000000000000444, 1.768423874527823347, -1.021000000000001018 ) ) ;
#20194=DIRECTION ( 'NONE',  ( 0.000000000000000000, 0.4999999999999993894, -0.8660254037844389297 ) ) ;
#20214=ORIENTED_EDGE ( 'NONE', *, *, #6329, .T. ) ;
#20263=ORIENTED_EDGE ( 'NONE', *, *, #10773, .T. ) ;
#20288=ORIENTED_EDGE ( 'NONE', *, *, #28524, .F. ) ;
#20305=ORIENTED_EDGE ( 'NONE', *, *, #27431, .F. ) ;
#20321=ORIENTED_EDGE ( 'NONE', *, *, #26868, .F. ) ;
#20461=ORIENTED_EDGE ( 'NONE', *, *, #5082, .F. ) ;
#20489=VERTEX_POINT ( 'NONE', #10696 ) ;
#20514=ORIENTED_EDGE ( 'NONE', *, *, #13312, .T. ) ;
#20536=ORIENTED_EDGE ( 'NONE', *, *, #24043, .F. ) ;
#20552=ORIENTED_EDGE ( 'NONE', *, *, #19821, .T. ) ;
#20574=ORIENTED_EDGE ( 'NONE', *, *, #12858, .T. ) ;
#20592=CIRCLE ( 'NONE', #25005, 2.055000000000000160 ) ;
#20608=EDGE_LOOP ( 'NONE', ( #13467, #23947, #18219, #12388 ) ) ;
#20618=FACE_OUTER_BOUND ( 'NONE', #15093, .T. ) ;
#20705=EDGE_CURVE ( 'NONE', #25132, #28670, #4726, .T. ) ;
#20729=CIRCLE ( 'NONE', #1772, 4.250000000000000000 ) ;
#20882=ADVANCED_FACE ( 'NONE', ( #11885 ), #7575, .T. ) ;
#20949=LINE ( 'NONE', #26156, #29124 ) ;
#20966=ORIENTED_EDGE ( 'NONE', *, *, #8459, .F. ) ;
#20969=AXIS2_PLACEMENT_3D ( 'NONE', #30243, #18879, #16281 ) ;
#21022=DIRECTION ( 'NONE',  ( -1.000000000000000000, 0.000000000000000000, 0.000000000000000000 ) ) ;
#21025=ADVANCED_FACE ( 'NONE', ( #1941 ), #24522, .F. ) ;
#21053=EDGE_LOOP ( 'NONE', ( #14552, #20552 ) ) ;
#21108=ORIENTED_EDGE ( 'NONE', *, *, #28303, .T. ) ;
#21121=VECTOR ( 'NONE', #3458, 1000.000000000000000 ) ;
#21165=AXIS2_PLACEMENT_3D ( 'NONE', #28767, #27345, #12681 ) ;
#21178=ORIENTED_EDGE ( 'NONE', *, *, #8690, .T. ) ;
#21210=CARTESIAN_POINT ( 'NONE',  ( 0.2500000000000002220, 4.898587196589412829E-16, -4.000000000000000000 ) ) ;
#21222=CARTESIAN_POINT ( 'NONE',  ( -31.74999999999995737, 5.204748896376250699E-16, -4.250000000000000000 ) ) ;
#21242=ORIENTED_EDGE ( 'NONE', *, *, #27363, .T. ) ;
#21307=ORIENTED_EDGE ( 'NONE', *, *, #21448, .T. ) ;
#21433=PLANE ( 'NONE',  #8023 ) ;
#21448=EDGE_CURVE ( 'NONE', #22950, #16768, #28111, .T. ) ;
#21480=CIRCLE ( 'NONE', #13682, 2.700000000000001066 ) ;
#21500=VECTOR ( 'NONE', #22195, 999.9999999999998863 ) ;
#21517=ADVANCED_FACE ( 'NONE', ( #19889 ), #5871, .F. ) ;
#21579=CIRCLE ( 'NONE', #23523, 2.041999999999999815 ) ;
#21583=CARTESIAN_POINT ( 'NONE',  ( 0.000000000000000000, -1.178949249685215417, 2.042000000000002036 ) ) ;
#21637=AXIS2_PLACEMENT_3D ( 'NONE', #11809, #29907, #25268 ) ;
#21739=CARTESIAN_POINT ( 'NONE',  ( 5.200000000000002842, 0.000000000000000000, 0.000000000000000000 ) ) ;
#21782=ORIENTED_EDGE ( 'NONE', *, *, #21448, .F. ) ;
#21787=ORIENTED_EDGE ( 'NONE', *, *, #22835, .T. ) ;
#21852=CARTESIAN_POINT ( 'NONE',  ( -31.74999999999995737, 0.000000000000000000, 0.000000000000000000 ) ) ;
#21866=LINE ( 'NONE', #20025, #26259 ) ;
#21912=ORIENTED_EDGE ( 'NONE', *, *, #1004, .F. ) ;
#21921=AXIS2_PLACEMENT_3D ( 'NONE', #25951, #7622, #19212 ) ;
#21940=ORIENTED_EDGE ( 'NONE', *, *, #16736, .T. ) ;
#21972=ORIENTED_EDGE ( 'NONE', *, *, #9203, .T. ) ;
#21980=CARTESIAN_POINT ( 'NONE',  ( 2.500000000000000444, -2.357898499370430834, 3.469446951953614189E-15 ) ) ;
#21991=( GEOMETRIC_REPRESENTATION_CONTEXT ( 3 ) GLOBAL_UNCERTAINTY_ASSIGNED_CONTEXT ( ( #22945 ) ) GLOBAL_UNIT_ASSIGNED_CONTEXT ( ( #3412, #23878, #976 ) ) REPRESENTATION_CONTEXT ( 'NONE', 'WORKASPACE' ) );
#22006=CONICAL_SURFACE ( 'NONE', #19086, 2.055000000000000160, 0.7853981633974721488 ) ;
#22024=( LENGTH_UNIT ( ) NAMED_UNIT ( * ) SI_UNIT ( .MILLI., .METRE. ) );
#22068=AXIS2_PLACEMENT_3D ( 'NONE', #12177, #9578, #16302 ) ;
#22134=DIRECTION ( 'NONE',  ( 0.000000000000000000, 0.000000000000000000, 1.000000000000000000 ) ) ;
#22173=DIRECTION ( 'NONE',  ( 0.000000000000000000, 0.000000000000000000, 1.000000000000000000 ) ) ;
#22195=DIRECTION ( 'NONE',  ( 0.000000000000000000, -0.5000000000000012212, -0.8660254037844380415 ) ) ;
#22235=LINE ( 'NONE', #26384, #5408 ) ;
#22267=CONICAL_SURFACE ( 'NONE', #14930, 2.041999999999999815, 1.047197551196591858 ) ;
#22348=FILL_AREA_STYLE_COLOUR ( '', #15103 ) ;
#22376=DIRECTION ( 'NONE',  ( -1.000000000000000000, 0.000000000000000000, 0.000000000000000000 ) ) ;
#22465=VERTEX_POINT ( 'NONE', #7662 ) ;
#22496=EDGE_CURVE ( 'NONE', #1053, #28447, #3390, .T. ) ;
#22563=CIRCLE ( 'NONE', #7918, 2.041999999999999815 ) ;
#22598=VERTEX_POINT ( 'NONE', #29213 ) ;
#22613=LINE ( 'NONE', #8705, #8795 ) ;
#22673=DIRECTION ( 'NONE',  ( 0.000000000000000000, 0.000000000000000000, -1.000000000000000000 ) ) ;
#22802=CARTESIAN_POINT ( 'NONE',  ( 0.000000000000000000, 1.178949249685215417, -2.042000000000002036 ) ) ;
#22816=ORIENTED_EDGE ( 'NONE', *, *, #20076, .F. ) ;
#22835=EDGE_CURVE ( 'NONE', #26603, #27706, #9511, .T. ) ;
#22838=DIRECTION ( 'NONE',  ( 0.000000000000000000, 0.000000000000000000, -1.000000000000000000 ) ) ;
#22882=CARTESIAN_POINT ( 'NONE',  ( 0.2500000000000002220, 0.000000000000000000, 4.000000000000000000 ) ) ;
#22937=CIRCLE ( 'NONE', #9746, 0.2000000000000000944 ) ;
#22945=UNCERTAINTY_MEASURE_WITH_UNIT (LENGTH_MEASURE( 1.000000000000000082E-05 ), #3412, 'distance_accuracy_value', 'NONE');
#22950=VERTEX_POINT ( 'NONE', #5305 ) ;
#22960=COLOUR_RGB ( '', 0.40784314, 0.44705882, 0.49803922) ;
#22962=DIRECTION ( 'NONE',  ( 0.000000000000000000, 0.000000000000000000, -1.000000000000000000 ) ) ;
#22993=EDGE_LOOP ( 'NONE', ( #16815, #3797, #21178, #27319, #19046 ) ) ;
#23057=DIRECTION ( 'NONE',  ( 0.000000000000000000, 0.000000000000000000, 1.000000000000000000 ) ) ;
#23099=DIRECTION ( 'NONE',  ( 0.000000000000000000, 1.000000000000000000, -1.224646799147353207E-16 ) ) ;
#23100=LINE ( 'NONE', #22802, #10803 ) ;
#23111=ORIENTED_EDGE ( 'NONE', *, *, #7198, .T. ) ;
#23121=FACE_OUTER_BOUND ( 'NONE', #16203, .T. ) ;
#23130=DIRECTION ( 'NONE',  ( 0.000000000000000000, 0.4999999999999993339, -0.8660254037844390407 ) ) ;
#23138=DIRECTION ( 'NONE',  ( -1.000000000000000000, 0.000000000000000000, 0.000000000000000000 ) ) ;
#23153=VERTEX_POINT ( 'NONE', #20092 ) ;
#23190=ADVANCED_FACE ( 'NONE', ( #3331 ), #15953, .T. ) ;
#23261=CARTESIAN_POINT ( 'NONE',  ( 5.000000000000002665, 3.306546357697854226E-16, 2.700000000000001066 ) ) ;
#23278=VECTOR ( 'NONE', #13636, 1000.000000000000000 ) ;
#23350=DIRECTION ( 'NONE',  ( -1.000000000000000000, 0.000000000000000000, 0.000000000000000000 ) ) ;
#23523=AXIS2_PLACEMENT_3D ( 'NONE', #7803, #19389, #22134 ) ;
#23613=LINE ( 'NONE', #25753, #14603 ) ;
#23620=DIRECTION ( 'NONE',  ( 0.000000000000000000, -0.4999999999999992784, 0.8660254037844389297 ) ) ;
#23658=FACE_BOUND ( 'NONE', #7663, .T. ) ;
#23781=DIRECTION ( 'NONE',  ( 0.000000000000000000, 0.000000000000000000, 1.000000000000000000 ) ) ;
#23876=CARTESIAN_POINT ( 'NONE',  ( 2.500000000000000444, 0.000000000000000000, 0.000000000000000000 ) ) ;
#23878=( NAMED_UNIT ( * ) PLANE_ANGLE_UNIT ( ) SI_UNIT ( $, .RADIAN. ) );
#23943=EDGE_LOOP ( 'NONE', ( #23111, #12465, #3682, #24440, #1541 ) ) ;
#23947=ORIENTED_EDGE ( 'NONE', *, *, #26436, .T. ) ;
#23963=LINE ( 'NONE', #12029, #14070 ) ;
#23975=DIRECTION ( 'NONE',  ( 0.000000000000000000, 0.000000000000000000, 1.000000000000000000 ) ) ;
#24008=PLANE ( 'NONE',  #21165 ) ;
#24032=CARTESIAN_POINT ( 'NONE',  ( 5.200000000000002842, 3.061616997868384127E-16, -2.500000000000000888 ) ) ;
#24043=EDGE_CURVE ( 'NONE', #10839, #28371, #20949, .T. ) ;
#24087=DIRECTION ( 'NONE',  ( -0.7071067811865306973, 8.659560562355138702E-17, -0.7071067811865643371 ) ) ;
#24173=ORIENTED_EDGE ( 'NONE', *, *, #8690, .F. ) ;
#24190=ORIENTED_EDGE ( 'NONE', *, *, #19821, .F. ) ;
#24196=SURFACE_SIDE_STYLE ('',( #17606 ) ) ;
#24283=ADVANCED_FACE ( 'NONE', ( #28928 ), #24604, .F. ) ;
#24293=CARTESIAN_POINT ( 'NONE',  ( 2.500000000000000444, -1.178949249685215417, 2.042000000000002036 ) ) ;
#24337=DIRECTION ( 'NONE',  ( 1.000000000000000000, 0.000000000000000000, 0.000000000000000000 ) ) ;
#24358=EDGE_CURVE ( 'NONE', #26561, #1053, #10246, .T. ) ;
#24364=EDGE_LOOP ( 'NONE', ( #7289, #12084, #21787, #24190 ) ) ;
#24440=ORIENTED_EDGE ( 'NONE', *, *, #7498, .F. ) ;
#24474=DIRECTION ( 'NONE',  ( -0.5000000000000051070, 0.000000000000000000, 0.8660254037844355990 ) ) ;
#24522=PLANE ( 'NONE',  #25142 ) ;
#24580=DIRECTION ( 'NONE',  ( -1.000000000000000000, 0.000000000000000000, 0.000000000000000000 ) ) ;
#24604=PLANE ( 'NONE',  #17838 ) ;
#24818=LINE ( 'NONE', #5900, #21121 ) ;
#24878=FACE_OUTER_BOUND ( 'NONE', #18714, .T. ) ;
#24994=ORIENTED_EDGE ( 'NONE', *, *, #28524, .T. ) ;
#25005=AXIS2_PLACEMENT_3D ( 'NONE', #17145, #19129, #5096 ) ;
#25041=CARTESIAN_POINT ( 'NONE',  ( 2.500000000000000444, 2.357898499370430834, -3.469446951953614189E-15 ) ) ;
#25064=DIRECTION ( 'NONE',  ( 1.000000000000000000, 0.000000000000000000, 0.000000000000000000 ) ) ;
#25074=LINE ( 'NONE', #8434, #15936 ) ;
#25076=DIRECTION ( 'NONE',  ( -1.000000000000000000, 0.000000000000000000, 0.000000000000000000 ) ) ;
#25125=CARTESIAN_POINT ( 'NONE',  ( 2.500000000000000444, -1.768423874527823347, -1.020999999999997687 ) ) ;
#25130=CARTESIAN_POINT ( 'NONE',  ( -31.74999999999995737, 0.000000000000000000, 0.000000000000000000 ) ) ;
#25132=VERTEX_POINT ( 'NONE', #2729 ) ;
#25142=AXIS2_PLACEMENT_3D ( 'NONE', #15653, #13216, #22838 ) ;
#25174=EDGE_LOOP ( 'NONE', ( #1133, #9812, #26453, #3844, #9723 ) ) ;
#25205=CARTESIAN_POINT ( 'NONE',  ( 2.500000000000000444, 0.000000000000000000, 0.000000000000000000 ) ) ;
#25240=FACE_OUTER_BOUND ( 'NONE', #22993, .T. ) ;
#25268=DIRECTION ( 'NONE',  ( 0.000000000000000000, 0.000000000000000000, -1.000000000000000000 ) ) ;
#25299=VECTOR ( 'NONE', #6046, 1000.000000000000114 ) ;
#25307=ORIENTED_EDGE ( 'NONE', *, *, #26868, .T. ) ;
#25323=EDGE_LOOP ( 'NONE', ( #12294, #30086, #17381, #11588, #3992 ) ) ;
#25342=CARTESIAN_POINT ( 'NONE',  ( 2.500000000000000444, -1.768423874527823347, 1.021000000000001018 ) ) ;
#25382=( GEOMETRIC_REPRESENTATION_CONTEXT ( 3 ) GLOBAL_UNCERTAINTY_ASSIGNED_CONTEXT ( ( #27261 ) ) GLOBAL_UNIT_ASSIGNED_CONTEXT ( ( #15008, #3585, #8299 ) ) REPRESENTATION_CONTEXT ( 'NONE', 'WORKASPACE' ) );
#25416=PLANE ( 'NONE',  #21637 ) ;
#25494=VERTEX_POINT ( 'NONE', #17904 ) ;
#25611=ORIENTED_EDGE ( 'NONE', *, *, #20076, .T. ) ;
#25658=EDGE_CURVE ( 'NONE', #14105, #22950, #13338, .T. ) ;
#25677=PRODUCT_DEFINITION_CONTEXT ( 'detailed design', #13390, 'design' ) ;
#25711=DIRECTION ( 'NONE',  ( 1.000000000000000000, 0.000000000000000000, 0.000000000000000000 ) ) ;
#25728=CARTESIAN_POINT ( 'NONE',  ( 2.500000000000000444, 0.000000000000000000, -2.041999999999998483 ) ) ;
#25753=CARTESIAN_POINT ( 'NONE',  ( 0.000000000000000000, -1.178949249685215417, 2.042000000000002036 ) ) ;
#25818=LINE ( 'NONE', #21222, #28204 ) ;
#25932=DIRECTION ( 'NONE',  ( 0.000000000000000000, 0.8660254037844380415, -0.5000000000000011102 ) ) ;
#25951=CARTESIAN_POINT ( 'NONE',  ( 0.000000000000000000, 0.000000000000000000, 0.000000000000000000 ) ) ;
#25961=EDGE_LOOP ( 'NONE', ( #19277, #1227, #5284, #15064 ) ) ;
#26056=VERTEX_POINT ( 'NONE', #8267 ) ;
#26059=DIRECTION ( 'NONE',  ( 0.000000000000000000, 0.8660254037844380415, -0.5000000000000012212 ) ) ;
#26073=PLANE ( 'NONE',  #2448 ) ;
#26089=ADVANCED_FACE ( 'NONE', ( #20618 ), #13749, .F. ) ;
#26131=AXIS2_PLACEMENT_3D ( 'NONE', #22882, #1985, #14444 ) ;
#26139=AXIS2_PLACEMENT_3D ( 'NONE', #11674, #23138, #11520 ) ;
#26149=AXIS2_PLACEMENT_3D ( 'NONE', #10129, #19441, #28957 ) ;
#26156=CARTESIAN_POINT ( 'NONE',  ( 2.500000000000000444, -2.357898499370430834, 3.469446951953614189E-15 ) ) ;
#26259=VECTOR ( 'NONE', #15134, 1000.000000000000000 ) ;
#26263=DIRECTION ( 'NONE',  ( 1.000000000000000000, -0.000000000000000000, -0.000000000000000000 ) ) ;
#26314=SURFACE_STYLE_USAGE ( .BOTH. , #16988 ) ;
#26338=CARTESIAN_POINT ( 'NONE',  ( 25.00000000000000000, 0.000000000000000000, 0.000000000000000000 ) ) ;
#26384=CARTESIAN_POINT ( 'NONE',  ( 25.00000000000000000, 2.516649172247811061E-16, -2.055000000000000160 ) ) ;
#26418=ORIENTED_EDGE ( 'NONE', *, *, #22496, .T. ) ;
#26436=EDGE_CURVE ( 'NONE', #6491, #29341, #25818, .T. ) ;
#26453=ORIENTED_EDGE ( 'NONE', *, *, #16728, .T. ) ;
#26454=CYLINDRICAL_SURFACE ( 'NONE', #9244, 4.250000000000000000 ) ;
#26516=CARTESIAN_POINT ( 'NONE',  ( -31.74999999999995737, 0.000000000000000000, 0.000000000000000000 ) ) ;
#26561=VERTEX_POINT ( 'NONE', #21980 ) ;
#26564=CIRCLE ( 'NONE', #15819, 4.250000000000000000 ) ;
#26603=VERTEX_POINT ( 'NONE', #29359 ) ;
#26621=SURFACE_STYLE_FILL_AREA ( #17286 ) ;
#26646=FILL_AREA_STYLE ('',( #22348 ) ) ;
#26692=ORIENTED_EDGE ( 'NONE', *, *, #106, .T. ) ;
#26715=ORIENTED_EDGE ( 'NONE', *, *, #8459, .T. ) ;
#26730=ORIENTED_EDGE ( 'NONE', *, *, #27431, .T. ) ;
#26787=EDGE_CURVE ( 'NONE', #1603, #16074, #8682, .T. ) ;
#26849=DIRECTION ( 'NONE',  ( 0.000000000000000000, 1.000000000000000000, 1.224646799147353207E-16 ) ) ;
#26868=EDGE_CURVE ( 'NONE', #28371, #28447, #19050, .T. ) ;
#26921=VERTEX_POINT ( 'NONE', #16763 ) ;
#26942=CIRCLE ( 'NONE', #22068, 2.055000000000000160 ) ;
#27220=DIRECTION ( 'NONE',  ( -1.000000000000000000, 0.000000000000000000, 0.000000000000000000 ) ) ;
#27261=UNCERTAINTY_MEASURE_WITH_UNIT (LENGTH_MEASURE( 1.000000000000000082E-05 ), #15008, 'distance_accuracy_value', 'NONE');
#27319=ORIENTED_EDGE ( 'NONE', *, *, #16270, .T. ) ;
#27345=DIRECTION ( 'NONE',  ( 1.000000000000000000, 0.000000000000000000, 0.000000000000000000 ) ) ;
#27363=EDGE_CURVE ( 'NONE', #27772, #1053, #17950, .T. ) ;
#27373=CARTESIAN_POINT ( 'NONE',  ( 25.00000000000000000, 0.000000000000000000, 0.000000000000000000 ) ) ;
#27405=VECTOR ( 'NONE', #23130, 1000.000000000000000 ) ;
#27409=DIRECTION ( 'NONE',  ( 0.000000000000000000, 0.000000000000000000, 1.000000000000000000 ) ) ;
#27431=EDGE_CURVE ( 'NONE', #3757, #14105, #30223, .T. ) ;
#27455=PRODUCT_DEFINITION ( 'UNKNOWN', '', #8752, #25677 ) ;
#27566=ORIENTED_EDGE ( 'NONE', *, *, #4317, .T. ) ;
#27701=AXIS2_PLACEMENT_3D ( 'NONE', #6756, #30165, #4312 ) ;
#27703=DIRECTION ( 'NONE',  ( -1.000000000000000000, 0.000000000000000000, 0.000000000000000000 ) ) ;
#27706=VERTEX_POINT ( 'NONE', #14841 ) ;
#27719=AXIS2_PLACEMENT_3D ( 'NONE', #15738, #25064, #4152 ) ;
#27742=AXIS2_PLACEMENT_3D ( 'NONE', #16611, #25932, #5014 ) ;
#27772=VERTEX_POINT ( 'NONE', #21583 ) ;
#27782=ORIENTED_EDGE ( 'NONE', *, *, #11404, .T. ) ;
#27866=AXIS2_PLACEMENT_3D ( 'NONE', #2055, #11335, #20194 ) ;
#27878=DIRECTION ( 'NONE',  ( 0.000000000000000000, -0.5000000000000012212, -0.8660254037844380415 ) ) ;
#27902=CARTESIAN_POINT ( 'NONE',  ( 2.500000000000000444, -2.357898499370430834, 3.469446951953614189E-15 ) ) ;
#27968=DIRECTION ( 'NONE',  ( 0.000000000000000000, -0.5000000000000011102, -0.8660254037844379305 ) ) ;
#27996=ADVANCED_FACE ( 'NONE', ( #4313 ), #1894, .T. ) ;
#28111=CIRCLE ( 'NONE', #26149, 2.500000000000000888 ) ;
#28124=ORIENTED_EDGE ( 'NONE', *, *, #7498, .T. ) ;
#28204=VECTOR ( 'NONE', #24580, 1000.000000000000000 ) ;
#28256=FACE_OUTER_BOUND ( 'NONE', #25323, .T. ) ;
#28303=EDGE_CURVE ( 'NONE', #25132, #1603, #10080, .T. ) ;
#28346=CARTESIAN_POINT ( 'NONE',  ( 0.000000000000000000, 1.178949249685215417, 2.041999999999998483 ) ) ;
#28371=VERTEX_POINT ( 'NONE', #14955 ) ;
#28421=EDGE_LOOP ( 'NONE', ( #21782, #19335, #2509, #20461 ) ) ;
#28447=VERTEX_POINT ( 'NONE', #17700 ) ;
#28524=EDGE_CURVE ( 'NONE', #11088, #28371, #17113, .T. ) ;
#28551=CIRCLE ( 'NONE', #29530, 4.250000000000000000 ) ;
#28623=EDGE_CURVE ( 'NONE', #23153, #11088, #14584, .T. ) ;
#28670=VERTEX_POINT ( 'NONE', #25342 ) ;
#28748=ORIENTED_EDGE ( 'NONE', *, *, #26436, .F. ) ;
#28752=ORIENTED_EDGE ( 'NONE', *, *, #12858, .F. ) ;
#28767=CARTESIAN_POINT ( 'NONE',  ( 2.500000000000000444, 2.357898499370430834, -3.469446951953614189E-15 ) ) ;
#28770=ORIENTED_EDGE ( 'NONE', *, *, #16728, .F. ) ;
#28804=ADVANCED_FACE ( 'NONE', ( #23658, #10049 ), #2760, .T. ) ;
#28842=EDGE_CURVE ( 'NONE', #14105, #3757, #13133, .T. ) ;
#28928=FACE_OUTER_BOUND ( 'NONE', #5311, .T. ) ;
#28950=DIRECTION ( 'NONE',  ( 1.000000000000000000, 0.000000000000000000, 0.000000000000000000 ) ) ;
#28957=DIRECTION ( 'NONE',  ( 0.000000000000000000, 0.000000000000000000, -1.000000000000000000 ) ) ;
#28958=DIRECTION ( 'NONE',  ( -1.000000000000000000, 0.000000000000000000, 0.000000000000000000 ) ) ;
#28959=DIRECTION ( 'NONE',  ( 0.000000000000000000, 0.000000000000000000, -1.000000000000000000 ) ) ;
#29060=CIRCLE ( 'NONE', #10007, 2.700000000000001066 ) ;
#29095=LINE ( 'NONE', #8134, #14763 ) ;
#29106=FACE_OUTER_BOUND ( 'NONE', #15917, .T. ) ;
#29124=VECTOR ( 'NONE', #16528, 1000.000000000000000 ) ;
#29167=ADVANCED_FACE ( 'NONE', ( #9562 ), #26073, .T. ) ;
#29171=ADVANCED_FACE ( 'NONE', ( #9257 ), #1951, .F. ) ;
#29213=CARTESIAN_POINT ( 'NONE',  ( 0.000000000000000000, 1.178949249685215417, -2.042000000000002036 ) ) ;
#29291=CARTESIAN_POINT ( 'NONE',  ( 0.000000000000000000, 2.357898499370430834, -3.469446951953614189E-15 ) ) ;
#29300=TOROIDAL_SURFACE ( 'NONE', #17, 2.700000000000001066, 0.2000000000000000111 ) ;
#29341=VERTEX_POINT ( 'NONE', #720 ) ;
#29359=CARTESIAN_POINT ( 'NONE',  ( 0.2500000000000002220, 0.000000000000000000, 4.250000000000000000 ) ) ;
#29371=FACE_OUTER_BOUND ( 'NONE', #5793, .T. ) ;
#29421=CARTESIAN_POINT ( 'NONE',  ( 2.500000000000000444, 2.357898499370430834, -3.469446951953614189E-15 ) ) ;
#29530=AXIS2_PLACEMENT_3D ( 'NONE', #14054, #27703, #27409 ) ;
#29540=DIRECTION ( 'NONE',  ( -1.000000000000000000, 0.000000000000000000, 0.000000000000000000 ) ) ;
#29566=DIRECTION ( 'NONE',  ( -1.000000000000000000, 0.000000000000000000, 0.000000000000000000 ) ) ;
#29625=DIRECTION ( 'NONE',  ( -1.000000000000000000, 0.000000000000000000, 0.000000000000000000 ) ) ;
#29752=ADVANCED_FACE ( 'NONE', ( #14818 ), #26454, .T. ) ;
#29768=DIRECTION ( 'NONE',  ( -1.000000000000000000, -0.000000000000000000, -0.000000000000000000 ) ) ;
#29840=CARTESIAN_POINT ( 'NONE',  ( 2.500000000000000444, 0.000000000000000000, 0.000000000000000000 ) ) ;
#29907=DIRECTION ( 'NONE',  ( 1.000000000000000000, 0.000000000000000000, 0.000000000000000000 ) ) ;
#30022=CARTESIAN_POINT ( 'NONE',  ( 5.200000000000002842, 3.306546357697854719E-16, 2.700000000000001066 ) ) ;
#30086=ORIENTED_EDGE ( 'NONE', *, *, #17750, .F. ) ;
#30094=AXIS2_PLACEMENT_3D ( 'NONE', #29421, #19735, #8588 ) ;
#30113=DIRECTION ( 'NONE',  ( 0.000000000000000000, 1.000000000000000000, -1.471414886128461471E-15 ) ) ;
#30114=CARTESIAN_POINT ( 'NONE',  ( 2.500000000000000444, 1.178949249685215417, 2.041999999999998483 ) ) ;
#30165=DIRECTION ( 'NONE',  ( -1.000000000000000000, 0.000000000000000000, 0.000000000000000000 ) ) ;
#30223=CIRCLE ( 'NONE', #18457, 2.500000000000001332 ) ;
#30243=CARTESIAN_POINT ( 'NONE',  ( 2.500000000000000444, -1.178949249685215417, 2.042000000000002036 ) ) ;
ENDSEC;
END-ISO-10303-21;
